ISO-10303-21;
HEADER;
FILE_DESCRIPTION (('STEP AP214'),
    '1' );
FILE_NAME ('Chuck Body Assembly Bolts.step',
    '2026-10-09T08:48:44',
    ( '' ),
    ( '' ),
    'SwSTEP 2.0',
    'SolidWorks 2026',
    '' );
FILE_SCHEMA (( 'AUTOMOTIVE_DESIGN' ));
ENDSEC;

DATA;
#80=VERTEX_POINT ( 'NONE', #70589 ) ;
#156=ADVANCED_FACE ( 'NONE', ( #41522 ), #80675, .F. ) ;
#344=CLOSED_SHELL ( 'NONE', ( #79052, #33768, #52211, #21587, #26399, #17656, #70205, #46060, #62381, #39288, #25788, #19324, #81414, #28723, #19290, #156, #10629, #6095, #46496, #61602, #656, #8490, #16295, #73331, #72597, #52522, #44952 ) ) ;
#467=CIRCLE ( 'NONE', #4492, 0.1181102362204724116 ) ;
#535=AXIS2_PLACEMENT_3D ( 'NONE', #45483, #71180, #13522 ) ;
#617=ORIENTED_EDGE ( 'NONE', *, *, #783, .T. ) ;
#633=DIRECTION ( 'NONE',  ( -1.000000000000000000, 1.445602896647338917E-16, -0.000000000000000000 ) ) ;
#656=ADVANCED_FACE ( 'NONE', ( #5775 ), #70162, .T. ) ;
#663=AXIS2_PLACEMENT_3D ( 'NONE', #18331, #57428, #5275 ) ;
#672=EDGE_CURVE ( 'NONE', #11621, #29401, #37361, .T. ) ;
#783=EDGE_CURVE ( 'NONE', #80, #29401, #36528, .T. ) ;
#845=EDGE_CURVE ( 'NONE', #15186, #5577, #75262, .T. ) ;
#914=ORIENTED_EDGE ( 'NONE', *, *, #4017, .T. ) ;
#920=FACE_OUTER_BOUND ( 'NONE', #64636, .T. ) ;
#953=VECTOR ( 'NONE', #10670, 39.37007874015748143 ) ;
#1111=DIRECTION ( 'NONE',  ( -1.000000000000000000, 1.445602896647338917E-16, -0.000000000000000000 ) ) ;
#1141=ORIENTED_EDGE ( 'NONE', *, *, #845, .F. ) ;
#1414=PLANE ( 'NONE',  #32563 ) ;
#1509=ORIENTED_EDGE ( 'NONE', *, *, #33244, .T. ) ;
#1590=LINE ( 'NONE', #65978, #22329 ) ;
#1605=FACE_OUTER_BOUND ( 'NONE', #33008, .T. ) ;
#1627=CARTESIAN_POINT ( 'NONE',  ( 0.1181102362204724532, 0.09842519685039372024, 0.000000000000000000 ) ) ;
#1636=ORIENTED_EDGE ( 'NONE', *, *, #46095, .T. ) ;
#1864=ORIENTED_EDGE ( 'NONE', *, *, #35126, .T. ) ;
#2033=PRODUCT_DEFINITION_FORMATION_WITH_SPECIFIED_SOURCE ( 'ANY', '', #59425, .NOT_KNOWN. ) ;
#2101=DIRECTION ( 'NONE',  ( 0.7071067811865474617, 0.000000000000000000, -0.7071067811865474617 ) ) ;
#2107=AXIS2_PLACEMENT_3D ( 'NONE', #62108, #62940, #23802 ) ;
#2148=EDGE_LOOP ( 'NONE', ( #71417, #20240, #3302, #914 ) ) ;
#2289=PRESENTATION_STYLE_ASSIGNMENT (( #48543 ) ) ;
#2384=EDGE_LOOP ( 'NONE', ( #24775, #59378, #3391, #53814 ) ) ;
#2388=VECTOR ( 'NONE', #42915, 39.37007874015748854 ) ;
#2406=DIRECTION ( 'NONE',  ( 0.000000000000000000, 0.000000000000000000, 1.000000000000000000 ) ) ;
#2433=CARTESIAN_POINT ( 'NONE',  ( 0.1181102362204724532, -0.09842519685039369248, 5.158493410915829266E-18 ) ) ;
#2563=DIRECTION ( 'NONE',  ( -1.332267629550188539E-16, -1.000000000000000000, 0.000000000000000000 ) ) ;
#2708=ORIENTED_EDGE ( 'NONE', *, *, #73731, .T. ) ;
#2791=CONICAL_SURFACE ( 'NONE', #82100, 0.1181102362204724116, 0.7853981633974536081 ) ;
#2911=AXIS2_PLACEMENT_3D ( 'NONE', #35097, #47712, #60355 ) ;
#3040=DIRECTION ( 'NONE',  ( -1.000000000000000000, -0.000000000000000000, -0.000000000000000000 ) ) ;
#3137=CIRCLE ( 'NONE', #71688, 0.09842519685039344268 ) ;
#3302=ORIENTED_EDGE ( 'NONE', *, *, #16262, .F. ) ;
#3343=CARTESIAN_POINT ( 'NONE',  ( 0.1181102362204724532, 0.09842519685039372024, 0.000000000000000000 ) ) ;
#3391=ORIENTED_EDGE ( 'NONE', *, *, #79579, .T. ) ;
#3648=CIRCLE ( 'NONE', #27856, 0.09842519685039372024 ) ;
#3654=CARTESIAN_POINT ( 'NONE',  ( 0.01968503937007875723, 0.000000000000000000, 0.1968503937007874405 ) ) ;
#3720=ORIENTED_EDGE ( 'NONE', *, *, #78379, .T. ) ;
#3940=ORIENTED_EDGE ( 'NONE', *, *, #47038, .T. ) ;
#3992=ORIENTED_EDGE ( 'NONE', *, *, #78629, .F. ) ;
#4017=EDGE_CURVE ( 'NONE', #77098, #48423, #4300, .T. ) ;
#4035=ORIENTED_EDGE ( 'NONE', *, *, #46544, .F. ) ;
#4300=LINE ( 'NONE', #55218, #80964 ) ;
#4372=LINE ( 'NONE', #30040, #53186 ) ;
#4469=CARTESIAN_POINT ( 'NONE',  ( 0.1181102362204724532, -0.09842519685039369248, 5.158493410915829266E-18 ) ) ;
#4492=AXIS2_PLACEMENT_3D ( 'NONE', #21782, #66834, #67655 ) ;
#4551=DIRECTION ( 'NONE',  ( 0.000000000000000000, 0.000000000000000000, 1.000000000000000000 ) ) ;
#4834=AXIS2_PLACEMENT_3D ( 'NONE', #13381, #39034, #29524 ) ;
#5008=CARTESIAN_POINT ( 'NONE',  ( 0.000000000000000000, 0.04921259842519689481, -0.08523872084492506440 ) ) ;
#5128=PLANE ( 'NONE',  #31473 ) ;
#5178=DIRECTION ( 'NONE',  ( -0.7071067811865437980, 0.000000000000000000, 0.7071067811865512365 ) ) ;
#5275=DIRECTION ( 'NONE',  ( 0.000000000000000000, 0.000000000000000000, 1.000000000000000000 ) ) ;
#5371=DIRECTION ( 'NONE',  ( 0.000000000000000000, 0.4999999999999998335, -0.8660254037844385966 ) ) ;
#5446=ORIENTED_EDGE ( 'NONE', *, *, #33065, .T. ) ;
#5577=VERTEX_POINT ( 'NONE', #67183 ) ;
#5590=STYLED_ITEM ( 'NONE', ( #2289 ), #33421 ) ;
#5690=CARTESIAN_POINT ( 'NONE',  ( 0.7086614173228347191, 0.000000000000000000, 0.000000000000000000 ) ) ;
#5775=FACE_OUTER_BOUND ( 'NONE', #69430, .T. ) ;
#5785=DIRECTION ( 'NONE',  ( 1.000000000000000000, 0.000000000000000000, 0.000000000000000000 ) ) ;
#5817=AXIS2_PLACEMENT_3D ( 'NONE', #26960, #54287, #8037 ) ;
#6093=CARTESIAN_POINT ( 'NONE',  ( 0.2362204724409449064, 0.000000000000000000, 0.1968503937007874405 ) ) ;
#6095=ADVANCED_FACE ( 'NONE', ( #52311 ), #1414, .F. ) ;
#6318=CARTESIAN_POINT ( 'NONE',  ( 0.1181102362204724254, 8.537024980200824098E-18, 0.000000000000000000 ) ) ;
#6352=PLANE ( 'NONE',  #9865 ) ;
#6402=EDGE_CURVE ( 'NONE', #29384, #60118, #28731, .T. ) ;
#6564=DIRECTION ( 'NONE',  ( -1.000000000000000000, -0.000000000000000000, -0.000000000000000000 ) ) ;
#6684=ORIENTED_EDGE ( 'NONE', *, *, #49555, .T. ) ;
#6818=DIRECTION ( 'NONE',  ( -1.734723475976806848E-16, -1.000000000000000000, 0.000000000000000000 ) ) ;
#6874=AXIS2_PLACEMENT_3D ( 'NONE', #1627, #39077, #32767 ) ;
#7106=ORIENTED_EDGE ( 'NONE', *, *, #79579, .F. ) ;
#7345=LINE ( 'NONE', #33013, #68750 ) ;
#7906=DIRECTION ( 'NONE',  ( -0.5144957554275267908, -0.8574929257125440962, 0.000000000000000000 ) ) ;
#7922=CARTESIAN_POINT ( 'NONE',  ( 0.1181102362204724532, 0.09842519685039372024, 0.000000000000000000 ) ) ;
#8037=DIRECTION ( 'NONE',  ( 0.000000000000000000, 0.000000000000000000, 1.000000000000000000 ) ) ;
#8185=DIRECTION ( 'NONE',  ( 0.000000000000000000, 0.000000000000000000, -1.000000000000000000 ) ) ;
#8194=FACE_OUTER_BOUND ( 'NONE', #12845, .T. ) ;
#8490=ADVANCED_FACE ( 'NONE', ( #71495 ), #39501, .T. ) ;
#8740=LINE ( 'NONE', #2433, #43986 ) ;
#8870=AXIS2_PLACEMENT_3D ( 'NONE', #68164, #42464, #17244 ) ;
#8998=CIRCLE ( 'NONE', #21133, 0.1771653543307086798 ) ;
#9051=VECTOR ( 'NONE', #9661, 39.37007874015748143 ) ;
#9136=CARTESIAN_POINT ( 'NONE',  ( 0.000000000000000000, 0.000000000000000000, 0.000000000000000000 ) ) ;
#9193=ORIENTED_EDGE ( 'NONE', *, *, #49555, .F. ) ;
#9364=FACE_OUTER_BOUND ( 'NONE', #76910, .T. ) ;
#9661=DIRECTION ( 'NONE',  ( 0.000000000000000000, 1.000000000000000000, -1.734723475976805862E-16 ) ) ;
#9672=CYLINDRICAL_SURFACE ( 'NONE', #8870, 0.1968503937007874405 ) ;
#9779=AXIS2_PLACEMENT_3D ( 'NONE', #16282, #66373, #29306 ) ;
#9842=FILL_AREA_STYLE ('',( #15337 ) ) ;
#9865=AXIS2_PLACEMENT_3D ( 'NONE', #70322, #38753, #12677 ) ;
#9987=CONICAL_SURFACE ( 'NONE', #77147, 0.1771653543307086798, 0.7853981633974482790 ) ;
#10052=ORIENTED_EDGE ( 'NONE', *, *, #13591, .F. ) ;
#10266=( NAMED_UNIT ( * ) SI_UNIT ( $, .STERADIAN. ) SOLID_ANGLE_UNIT ( ) );
#10280=AXIS2_PLACEMENT_3D ( 'NONE', #13681, #65021, #65453 ) ;
#10344=DIRECTION ( 'NONE',  ( -1.000000000000000000, -0.000000000000000000, -0.000000000000000000 ) ) ;
#10554=FACE_OUTER_BOUND ( 'NONE', #25320, .T. ) ;
#10629=ADVANCED_FACE ( 'NONE', ( #54979 ), #43576, .F. ) ;
#10670=DIRECTION ( 'NONE',  ( -1.000000000000000000, -0.000000000000000000, -0.000000000000000000 ) ) ;
#10681=CARTESIAN_POINT ( 'NONE',  ( 0.6889763779527560139, 0.000000000000000000, 0.1181102362204724116 ) ) ;
#10789=DIRECTION ( 'NONE',  ( -1.000000000000000000, 0.000000000000000000, -0.000000000000000000 ) ) ;
#11034=DIRECTION ( 'NONE',  ( -1.000000000000000000, -0.000000000000000000, -0.000000000000000000 ) ) ;
#11082=DIRECTION ( 'NONE',  ( -1.734723475976806848E-16, -1.000000000000000000, 0.000000000000000000 ) ) ;
#11163=DIRECTION ( 'NONE',  ( 0.000000000000000000, 0.000000000000000000, 1.000000000000000000 ) ) ;
#11284=DIRECTION ( 'NONE',  ( 1.445602896647338917E-16, 1.000000000000000000, 0.000000000000000000 ) ) ;
#11329=DIRECTION ( 'NONE',  ( 0.000000000000000000, -1.000000000000000000, 1.734723475976806108E-16 ) ) ;
#11621=VERTEX_POINT ( 'NONE', #53208 ) ;
#11639=AXIS2_PLACEMENT_3D ( 'NONE', #7922, #15906, #33583 ) ;
#11706=DIRECTION ( 'NONE',  ( -1.000000000000000000, -0.000000000000000000, -0.000000000000000000 ) ) ;
#11857=DIRECTION ( 'NONE',  ( -0.000000000000000000, 0.000000000000000000, 1.000000000000000000 ) ) ;
#12164=CARTESIAN_POINT ( 'NONE',  ( 0.000000000000000000, -0.04921259842519688094, 0.08523872084492505052 ) ) ;
#12579=ORIENTED_EDGE ( 'NONE', *, *, #783, .F. ) ;
#12662=CIRCLE ( 'NONE', #535, 0.1968503937007874405 ) ;
#12677=DIRECTION ( 'NONE',  ( 0.000000000000000000, 1.000000000000000000, -1.734723475976805862E-16 ) ) ;
#12679=APPLICATION_CONTEXT ( 'automotive_design' ) ;
#12845=EDGE_LOOP ( 'NONE', ( #74539, #1864, #40348, #76061, #80857 ) ) ;
#12849=FACE_OUTER_BOUND ( 'NONE', #24694, .T. ) ;
#12854=ORIENTED_EDGE ( 'NONE', *, *, #845, .T. ) ;
#13381=CARTESIAN_POINT ( 'NONE',  ( 0.01968503937007875723, 0.000000000000000000, 0.000000000000000000 ) ) ;
#13392=DIRECTION ( 'NONE',  ( 0.000000000000000000, 0.000000000000000000, 1.000000000000000000 ) ) ;
#13522=DIRECTION ( 'NONE',  ( 0.000000000000000000, 0.000000000000000000, 1.000000000000000000 ) ) ;
#13591=EDGE_CURVE ( 'NONE', #70661, #67145, #54367, .T. ) ;
#13665=ORIENTED_EDGE ( 'NONE', *, *, #46544, .T. ) ;
#13680=DIRECTION ( 'NONE',  ( -1.332267629550188539E-16, -1.000000000000000000, 0.000000000000000000 ) ) ;
#13681=CARTESIAN_POINT ( 'NONE',  ( 0.2460629921259842590, 0.000000000000000000, 0.000000000000000000 ) ) ;
#13852=EDGE_LOOP ( 'NONE', ( #39012, #43245 ) ) ;
#13878=VECTOR ( 'NONE', #14560, 39.37007874015748854 ) ;
#13901=CARTESIAN_POINT ( 'NONE',  ( 0.1181102362204724532, 0.04921259842519689481, 0.08523872084492503665 ) ) ;
#13955=VECTOR ( 'NONE', #55974, 39.37007874015748854 ) ;
#14261=ORIENTED_EDGE ( 'NONE', *, *, #52608, .F. ) ;
#14353=VECTOR ( 'NONE', #6564, 39.37007874015748143 ) ;
#14462=CARTESIAN_POINT ( 'NONE',  ( 0.000000000000000000, -0.04921259842519685318, -0.08523872084492505052 ) ) ;
#14513=DIRECTION ( 'NONE',  ( 0.000000000000000000, 0.000000000000000000, -1.000000000000000000 ) ) ;
#14560=DIRECTION ( 'NONE',  ( 0.000000000000000000, 0.4999999999999997224, 0.8660254037844388186 ) ) ;
#15186=VERTEX_POINT ( 'NONE', #51751 ) ;
#15246=EDGE_CURVE ( 'NONE', #47884, #66895, #3648, .T. ) ;
#15274=PLANE ( 'NONE',  #81422 ) ;
#15337=FILL_AREA_STYLE_COLOUR ( '', #59365 ) ;
#15616=CIRCLE ( 'NONE', #4834, 0.1968503937007874405 ) ;
#15760=SURFACE_SIDE_STYLE ('',( #41815 ) ) ;
#15906=DIRECTION ( 'NONE',  ( 1.000000000000000000, -1.445602896647338917E-16, 0.000000000000000000 ) ) ;
#16008=EDGE_CURVE ( 'NONE', #82474, #67145, #79139, .T. ) ;
#16047=PLANE ( 'NONE',  #30427 ) ;
#16262=EDGE_CURVE ( 'NONE', #77098, #51714, #73221, .T. ) ;
#16282=CARTESIAN_POINT ( 'NONE',  ( 0.1181102362204724532, -0.04921259842519688094, 0.08523872084492505052 ) ) ;
#16295=ADVANCED_FACE ( 'NONE', ( #35331 ), #60994, .T. ) ;
#16376=CIRCLE ( 'NONE', #2911, 0.09842519685039372024 ) ;
#16632=DIRECTION ( 'NONE',  ( 0.000000000000000000, 0.000000000000000000, 1.000000000000000000 ) ) ;
#16828=FACE_OUTER_BOUND ( 'NONE', #74750, .T. ) ;
#16859=DIRECTION ( 'NONE',  ( -1.000000000000000000, -0.000000000000000000, -0.000000000000000000 ) ) ;
#17052=ORIENTED_EDGE ( 'NONE', *, *, #672, .T. ) ;
#17151=VERTEX_POINT ( 'NONE', #14462 ) ;
#17244=DIRECTION ( 'NONE',  ( 0.000000000000000000, 0.000000000000000000, 1.000000000000000000 ) ) ;
#17248=DIRECTION ( 'NONE',  ( -1.000000000000000000, 1.445602896647338917E-16, -0.000000000000000000 ) ) ;
#17287=LINE ( 'NONE', #55960, #2388 ) ;
#17296=ORIENTED_EDGE ( 'NONE', *, *, #6402, .T. ) ;
#17525=LENGTH_MEASURE_WITH_UNIT ( LENGTH_MEASURE( 0.02539999999999999897 ), #54554 );
#17527=PLANE ( 'NONE',  #29077 ) ;
#17656=ADVANCED_FACE ( 'NONE', ( #58405 ), #51242, .T. ) ;
#17921=CARTESIAN_POINT ( 'NONE',  ( 0.000000000000000000, 0.000000000000000000, 0.1181102362204724116 ) ) ;
#17997=DIMENSIONAL_EXPONENTS ( 1.000000000000000000, 0.000000000000000000, 0.000000000000000000, 0.000000000000000000, 0.000000000000000000, 0.000000000000000000, 0.000000000000000000 ) ;
#18026=DIRECTION ( 'NONE',  ( 0.000000000000000000, 0.000000000000000000, -1.000000000000000000 ) ) ;
#18089=ORIENTED_EDGE ( 'NONE', *, *, #33244, .F. ) ;
#18308=EDGE_CURVE ( 'NONE', #66895, #22673, #8740, .T. ) ;
#18331=CARTESIAN_POINT ( 'NONE',  ( 0.2460629921259843422, 0.000000000000000000, 0.000000000000000000 ) ) ;
#18628=EDGE_LOOP ( 'NONE', ( #22659, #44271, #49560, #64784 ) ) ;
#18989=DIRECTION ( 'NONE',  ( 1.445602896647338917E-16, 1.000000000000000000, 0.000000000000000000 ) ) ;
#19290=ADVANCED_FACE ( 'NONE', ( #60700 ), #15274, .F. ) ;
#19317=CONICAL_SURFACE ( 'NONE', #71786, 65.61679790026244063, 1.030376826524312284 ) ;
#19324=ADVANCED_FACE ( 'NONE', ( #73768, #9364 ), #67442, .F. ) ;
#19606=LINE ( 'NONE', #70964, #14353 ) ;
#19733=ORIENTED_EDGE ( 'NONE', *, *, #18308, .T. ) ;
#19871=FACE_OUTER_BOUND ( 'NONE', #52135, .T. ) ;
#20049=EDGE_LOOP ( 'NONE', ( #39373, #60628, #5446, #56356 ) ) ;
#20238=FACE_OUTER_BOUND ( 'NONE', #38152, .T. ) ;
#20240=ORIENTED_EDGE ( 'NONE', *, *, #42687, .F. ) ;
#20445=EDGE_LOOP ( 'NONE', ( #48127, #21810 ) ) ;
#20564=EDGE_LOOP ( 'NONE', ( #79117, #3720, #49874, #65438 ) ) ;
#20623=VECTOR ( 'NONE', #44219, 39.37007874015748854 ) ;
#21086=FACE_OUTER_BOUND ( 'NONE', #63123, .T. ) ;
#21133=AXIS2_PLACEMENT_3D ( 'NONE', #82003, #82409, #18026 ) ;
#21219=ORIENTED_EDGE ( 'NONE', *, *, #59455, .T. ) ;
#21410=EDGE_CURVE ( 'NONE', #32372, #70661, #38374, .T. ) ;
#21587=ADVANCED_FACE ( 'NONE', ( #43145 ), #37264, .T. ) ;
#21730=CARTESIAN_POINT ( 'NONE',  ( 0.1181102362204724532, 0.04921259842519689481, -0.08523872084492506440 ) ) ;
#21782=CARTESIAN_POINT ( 'NONE',  ( 0.6889763779527560139, 0.000000000000000000, 0.000000000000000000 ) ) ;
#21810=ORIENTED_EDGE ( 'NONE', *, *, #29128, .F. ) ;
#22096=CARTESIAN_POINT ( 'NONE',  ( 0.1181102362204724532, -0.09842519685039369248, 5.158493410915829266E-18 ) ) ;
#22098=AXIS2_PLACEMENT_3D ( 'NONE', #9136, #2406, #28064 ) ;
#22329=VECTOR ( 'NONE', #7906, 39.37007874015748854 ) ;
#22470=DIRECTION ( 'NONE',  ( -1.000000000000000000, -0.000000000000000000, -0.000000000000000000 ) ) ;
#22659=ORIENTED_EDGE ( 'NONE', *, *, #22774, .F. ) ;
#22673=VERTEX_POINT ( 'NONE', #33441 ) ;
#22676=ORIENTED_EDGE ( 'NONE', *, *, #71970, .T. ) ;
#22774=EDGE_CURVE ( 'NONE', #62196, #82474, #63968, .T. ) ;
#22974=LINE ( 'NONE', #21730, #63718 ) ;
#23353=AXIS2_PLACEMENT_3D ( 'NONE', #74900, #17248, #43282 ) ;
#23368=PRODUCT_DEFINITION ( 'UNKNOWN', '', #2033, #63882 ) ;
#23600=AXIS2_PLACEMENT_3D ( 'NONE', #35447, #61941, #35035 ) ;
#23752=ORIENTED_EDGE ( 'NONE', *, *, #18308, .F. ) ;
#23802=DIRECTION ( 'NONE',  ( 0.000000000000000000, 0.000000000000000000, 1.000000000000000000 ) ) ;
#23827=DIRECTION ( 'NONE',  ( 0.000000000000000000, -0.4999999999999997224, -0.8660254037844388186 ) ) ;
#23848=DIRECTION ( 'NONE',  ( 0.000000000000000000, -1.224646799147351482E-16, 1.000000000000000000 ) ) ;
#23960=EDGE_LOOP ( 'NONE', ( #82490, #77946 ) ) ;
#24092=VECTOR ( 'NONE', #5371, 39.37007874015748854 ) ;
#24391=FACE_OUTER_BOUND ( 'NONE', #2384, .T. ) ;
#24498=CARTESIAN_POINT ( 'NONE',  ( 0.6889763779527560139, 0.000000000000000000, 0.1181102362204724116 ) ) ;
#24665=VECTOR ( 'NONE', #11329, 39.37007874015748143 ) ;
#24694=EDGE_LOOP ( 'NONE', ( #14261, #2708, #54030, #7106 ) ) ;
#24775=ORIENTED_EDGE ( 'NONE', *, *, #73731, .F. ) ;
#25002=DIRECTION ( 'NONE',  ( 0.000000000000000000, 0.000000000000000000, 1.000000000000000000 ) ) ;
#25320=EDGE_LOOP ( 'NONE', ( #41596, #33031 ) ) ;
#25702=VECTOR ( 'NONE', #5178, 39.37007874015748143 ) ;
#25788=ADVANCED_FACE ( 'NONE', ( #29720 ), #17527, .F. ) ;
#26024=CARTESIAN_POINT ( 'NONE',  ( 0.2362204724409449064, 0.000000000000000000, 0.1279527559055117503 ) ) ;
#26185=CIRCLE ( 'NONE', #663, 0.1181102362204723977 ) ;
#26399=ADVANCED_FACE ( 'NONE', ( #12849 ), #46540, .F. ) ;
#26426=CARTESIAN_POINT ( 'NONE',  ( 0.000000000000000000, 0.000000000000000000, 0.000000000000000000 ) ) ;
#26462=CIRCLE ( 'NONE', #74852, 0.09842519685039344268 ) ;
#26577=PLANE ( 'NONE',  #34647 ) ;
#26960=CARTESIAN_POINT ( 'NONE',  ( 0.2362204724409449064, 0.000000000000000000, 0.000000000000000000 ) ) ;
#27070=CARTESIAN_POINT ( 'NONE',  ( 0.1181102362204724532, -0.04921259842519685318, -0.08523872084492505052 ) ) ;
#27201=SHAPE_REPRESENTATION ( 'Chuck Body Assembly Bolts', ( #22098 ), #46360 ) ;
#27496=AXIS2_PLACEMENT_3D ( 'NONE', #32485, #40066, #34165 ) ;
#27801=DIRECTION ( 'NONE',  ( 0.000000000000000000, -0.4999999999999998890, 0.8660254037844385966 ) ) ;
#27856=AXIS2_PLACEMENT_3D ( 'NONE', #6318, #77454, #59332 ) ;
#28064=DIRECTION ( 'NONE',  ( 1.000000000000000000, 0.000000000000000000, 0.000000000000000000 ) ) ;
#28090=DIRECTION ( 'NONE',  ( -1.000000000000000000, -0.000000000000000000, -0.000000000000000000 ) ) ;
#28723=ADVANCED_FACE ( 'NONE', ( #35094 ), #2791, .T. ) ;
#28731=LINE ( 'NONE', #79688, #35285 ) ;
#28777=CARTESIAN_POINT ( 'NONE',  ( 0.6889763779527560139, 0.000000000000000000, 0.000000000000000000 ) ) ;
#29077=AXIS2_PLACEMENT_3D ( 'NONE', #5690, #10789, #43159 ) ;
#29118=AXIS2_PLACEMENT_3D ( 'NONE', #55820, #67654, #23848 ) ;
#29128=EDGE_CURVE ( 'NONE', #15186, #47884, #55213, .T. ) ;
#29130=CARTESIAN_POINT ( 'NONE',  ( 0.1181102362204724532, 0.04921259842519689481, 0.08523872084492503665 ) ) ;
#29153=ORIENTED_EDGE ( 'NONE', *, *, #74789, .F. ) ;
#29306=DIRECTION ( 'NONE',  ( 0.000000000000000000, -1.000000000000000000, 1.734723475976805615E-16 ) ) ;
#29310=( CONVERSION_BASED_UNIT ( 'INCH', #17525 ) LENGTH_UNIT ( ) NAMED_UNIT ( #50239 ) );
#29345=AXIS2_PLACEMENT_3D ( 'NONE', #58749, #1111, #38967 ) ;
#29384=VERTEX_POINT ( 'NONE', #54475 ) ;
#29401=VERTEX_POINT ( 'NONE', #78939 ) ;
#29524=DIRECTION ( 'NONE',  ( 0.000000000000000000, 0.000000000000000000, -1.000000000000000000 ) ) ;
#29602=DIRECTION ( 'NONE',  ( -1.000000000000000000, 1.445602896647338917E-16, -0.000000000000000000 ) ) ;
#29654=CARTESIAN_POINT ( 'NONE',  ( 0.2362204724409449064, 0.1279527559055118335, 0.000000000000000000 ) ) ;
#29720=FACE_OUTER_BOUND ( 'NONE', #42022, .T. ) ;
#30040=CARTESIAN_POINT ( 'NONE',  ( 1.080276388343102000E-18, 2.169649841009090648E-17, 0.1771653543307086798 ) ) ;
#30117=LINE ( 'NONE', #17921, #51697 ) ;
#30210=CARTESIAN_POINT ( 'NONE',  ( 0.1181102362204724532, 0.09842519685039372024, 0.000000000000000000 ) ) ;
#30272=VERTEX_POINT ( 'NONE', #26024 ) ;
#30427=AXIS2_PLACEMENT_3D ( 'NONE', #74947, #68615, #67386 ) ;
#30503=EDGE_CURVE ( 'NONE', #54019, #11621, #37829, .T. ) ;
#30842=CARTESIAN_POINT ( 'NONE',  ( 0.6889763779527560139, 0.000000000000000000, 0.000000000000000000 ) ) ;
#31115=CARTESIAN_POINT ( 'NONE',  ( 1.080276388343102000E-18, 2.290185943287373359E-17, 0.1771653543307086798 ) ) ;
#31223=ORIENTED_EDGE ( 'NONE', *, *, #16008, .T. ) ;
#31444=CARTESIAN_POINT ( 'NONE',  ( 0.000000000000000000, 0.04921259842519689481, 0.08523872084492503665 ) ) ;
#31456=ORIENTED_EDGE ( 'NONE', *, *, #47038, .F. ) ;
#31473=AXIS2_PLACEMENT_3D ( 'NONE', #69105, #69519, #18989 ) ;
#31503=LINE ( 'NONE', #12164, #46771 ) ;
#32285=VERTEX_POINT ( 'NONE', #36851 ) ;
#32372=VERTEX_POINT ( 'NONE', #6093 ) ;
#32462=CARTESIAN_POINT ( 'NONE',  ( 0.1181102362204724532, 0.09842519685039372024, -1.432673802628665356E-17 ) ) ;
#32485=CARTESIAN_POINT ( 'NONE',  ( 1.080276388343102000E-18, 0.000000000000000000, 0.000000000000000000 ) ) ;
#32563=AXIS2_PLACEMENT_3D ( 'NONE', #27070, #46419, #72111 ) ;
#32695=EDGE_CURVE ( 'NONE', #22673, #48423, #7345, .T. ) ;
#32767=DIRECTION ( 'NONE',  ( 1.445602896647338917E-16, 1.000000000000000000, 0.000000000000000000 ) ) ;
#33008=EDGE_LOOP ( 'NONE', ( #63631, #79786 ) ) ;
#33013=CARTESIAN_POINT ( 'NONE',  ( 0.000000000000000000, -0.09842519685039369248, 5.158493410915829266E-18 ) ) ;
#33031=ORIENTED_EDGE ( 'NONE', *, *, #60488, .F. ) ;
#33065=EDGE_CURVE ( 'NONE', #67145, #81967, #56647, .T. ) ;
#33144=AXIS2_PLACEMENT_3D ( 'NONE', #38052, #70041, #25002 ) ;
#33244=EDGE_CURVE ( 'NONE', #11621, #15186, #16376, .T. ) ;
#33343=DIRECTION ( 'NONE',  ( -1.000000000000000000, 1.445602896647338917E-16, -0.000000000000000000 ) ) ;
#33421=MANIFOLD_SOLID_BREP ( 'Cut-Revolve1', #344 ) ;
#33441=CARTESIAN_POINT ( 'NONE',  ( 0.000000000000000000, -0.09842519685039369248, 5.158493410915829266E-18 ) ) ;
#33583=DIRECTION ( 'NONE',  ( 1.445602896647338917E-16, 1.000000000000000000, 0.000000000000000000 ) ) ;
#33761=EDGE_CURVE ( 'NONE', #50299, #49469, #50599, .T. ) ;
#33768=ADVANCED_FACE ( 'NONE', ( #50193 ), #43187, .T. ) ;
#33826=CARTESIAN_POINT ( 'NONE',  ( 0.000000000000000000, -0.04921259842519688094, 0.08523872084492505052 ) ) ;
#34165=DIRECTION ( 'NONE',  ( 0.000000000000000000, 0.000000000000000000, -1.000000000000000000 ) ) ;
#34647=AXIS2_PLACEMENT_3D ( 'NONE', #32462, #44650, #77933 ) ;
#34666=EDGE_CURVE ( 'NONE', #81967, #67145, #15616, .T. ) ;
#35035=DIRECTION ( 'NONE',  ( 0.000000000000000000, 0.000000000000000000, -1.000000000000000000 ) ) ;
#35094=FACE_OUTER_BOUND ( 'NONE', #82702, .T. ) ;
#35097=CARTESIAN_POINT ( 'NONE',  ( 0.1181102362204724254, 8.537024980200824098E-18, 0.000000000000000000 ) ) ;
#35126=EDGE_CURVE ( 'NONE', #54019, #66895, #1590, .T. ) ;
#35146=FACE_OUTER_BOUND ( 'NONE', #23960, .T. ) ;
#35285=VECTOR ( 'NONE', #61126, 39.37007874015748143 ) ;
#35309=ORIENTED_EDGE ( 'NONE', *, *, #15246, .T. ) ;
#35331=FACE_OUTER_BOUND ( 'NONE', #20445, .T. ) ;
#35447=CARTESIAN_POINT ( 'NONE',  ( 1.080276388343102000E-18, 0.1968503937007874127, 0.000000000000000000 ) ) ;
#35466=CARTESIAN_POINT ( 'NONE',  ( 1.080276388343102000E-18, 0.000000000000000000, 0.000000000000000000 ) ) ;
#35509=CARTESIAN_POINT ( 'NONE',  ( 0.1181102362204724254, 8.537024980200824098E-18, 0.000000000000000000 ) ) ;
#35560=FACE_BOUND ( 'NONE', #37373, .T. ) ;
#35609=DIRECTION ( 'NONE',  ( 0.000000000000000000, -1.000000000000000000, 0.000000000000000000 ) ) ;
#35687=ORIENTED_EDGE ( 'NONE', *, *, #672, .F. ) ;
#35758=EDGE_CURVE ( 'NONE', #62196, #81967, #4372, .T. ) ;
#35799=DIRECTION ( 'NONE',  ( 0.000000000000000000, 0.000000000000000000, 1.000000000000000000 ) ) ;
#35907=VECTOR ( 'NONE', #2101, 39.37007874015748854 ) ;
#35911=CIRCLE ( 'NONE', #57385, 0.09842519685039372024 ) ;
#36178=VECTOR ( 'NONE', #11706, 39.37007874015748143 ) ;
#36528=LINE ( 'NONE', #31444, #24092 ) ;
#36851=CARTESIAN_POINT ( 'NONE',  ( 0.2362204724409449064, 1.566969329617675860E-17, -0.1279527559055117503 ) ) ;
#36996=AXIS2_PLACEMENT_3D ( 'NONE', #81899, #74339, #75581 ) ;
#37264=CYLINDRICAL_SURFACE ( 'NONE', #2107, 0.1181102362204724116 ) ;
#37361=LINE ( 'NONE', #44068, #36178 ) ;
#37373=EDGE_LOOP ( 'NONE', ( #42923, #64248 ) ) ;
#37436=ORIENTED_EDGE ( 'NONE', *, *, #55337, .F. ) ;
#37829=LINE ( 'NONE', #57170, #44504 ) ;
#38052=CARTESIAN_POINT ( 'NONE',  ( 0.000000000000000000, 0.000000000000000000, 0.000000000000000000 ) ) ;
#38152=EDGE_LOOP ( 'NONE', ( #59211, #47073, #48243, #12854 ) ) ;
#38374=CIRCLE ( 'NONE', #36996, 0.1968503937007874405 ) ;
#38488=ORIENTED_EDGE ( 'NONE', *, *, #56663, .F. ) ;
#38496=DIRECTION ( 'NONE',  ( 0.000000000000000000, 0.4999999999999997224, 0.8660254037844388186 ) ) ;
#38634=CARTESIAN_POINT ( 'NONE',  ( 0.2362204724409449064, 2.410722045565656378E-17, -0.1968503937007874405 ) ) ;
#38719=LINE ( 'NONE', #13901, #68912 ) ;
#38753=DIRECTION ( 'NONE',  ( 0.000000000000000000, -1.734723475976805862E-16, -1.000000000000000000 ) ) ;
#38885=FACE_OUTER_BOUND ( 'NONE', #20564, .T. ) ;
#38967=DIRECTION ( 'NONE',  ( -1.734723475976806848E-16, -1.000000000000000000, 0.000000000000000000 ) ) ;
#39012=ORIENTED_EDGE ( 'NONE', *, *, #16262, .T. ) ;
#39013=ORIENTED_EDGE ( 'NONE', *, *, #34666, .F. ) ;
#39034=DIRECTION ( 'NONE',  ( 1.000000000000000000, 0.000000000000000000, 0.000000000000000000 ) ) ;
#39057=EDGE_CURVE ( 'NONE', #80363, #60118, #41194, .T. ) ;
#39077=DIRECTION ( 'NONE',  ( 1.000000000000000000, -1.445602896647338917E-16, 0.000000000000000000 ) ) ;
#39288=ADVANCED_FACE ( 'NONE', ( #38885 ), #44759, .T. ) ;
#39373=ORIENTED_EDGE ( 'NONE', *, *, #21410, .T. ) ;
#39464=UNCERTAINTY_MEASURE_WITH_UNIT (LENGTH_MEASURE( 1.000000000000000082E-05 ), #73830, 'distance_accuracy_value', 'NONE');
#39501=PLANE ( 'NONE',  #6874 ) ;
#39510=EDGE_LOOP ( 'NONE', ( #6684, #18089 ) ) ;
#39607=DIRECTION ( 'NONE',  ( -1.000000000000000000, 1.445602896647338917E-16, -0.000000000000000000 ) ) ;
#40066=DIRECTION ( 'NONE',  ( 1.000000000000000000, 0.000000000000000000, 0.000000000000000000 ) ) ;
#40348=ORIENTED_EDGE ( 'NONE', *, *, #60488, .T. ) ;
#40415=EDGE_CURVE ( 'NONE', #50299, #53271, #26462, .T. ) ;
#40430=LINE ( 'NONE', #60615, #81077 ) ;
#40447=EDGE_CURVE ( 'NONE', #82474, #62196, #8998, .T. ) ;
#40910=CONICAL_SURFACE ( 'NONE', #27496, 0.1771653543307086798, 0.7853981633974482790 ) ;
#41194=CIRCLE ( 'NONE', #57323, 0.1181102362204723977 ) ;
#41522=FACE_OUTER_BOUND ( 'NONE', #2148, .T. ) ;
#41596=ORIENTED_EDGE ( 'NONE', *, *, #74789, .T. ) ;
#41815=SURFACE_STYLE_FILL_AREA ( #9842 ) ;
#41863=CARTESIAN_POINT ( 'NONE',  ( 0.7086614173228347191, 0.000000000000000000, 0.000000000000000000 ) ) ;
#41882=AXIS2_PLACEMENT_3D ( 'NONE', #65852, #51518, #8185 ) ;
#41892=ORIENTED_EDGE ( 'NONE', *, *, #40415, .F. ) ;
#42022=EDGE_LOOP ( 'NONE', ( #51606, #1636 ) ) ;
#42120=CIRCLE ( 'NONE', #5817, 0.1279527559055117503 ) ;
#42184=DIRECTION ( 'NONE',  ( 1.000000000000000000, 0.000000000000000000, 0.000000000000000000 ) ) ;
#42217=AXIS2_PLACEMENT_3D ( 'NONE', #73512, #35609, #65944 ) ;
#42231=( LENGTH_UNIT ( ) NAMED_UNIT ( * ) SI_UNIT ( $, .METRE. ) );
#42464=DIRECTION ( 'NONE',  ( -1.000000000000000000, -0.000000000000000000, -0.000000000000000000 ) ) ;
#42687=EDGE_CURVE ( 'NONE', #51714, #80, #38719, .T. ) ;
#42915=DIRECTION ( 'NONE',  ( 0.000000000000000000, -0.4999999999999998890, 0.8660254037844385966 ) ) ;
#42923=ORIENTED_EDGE ( 'NONE', *, *, #46991, .T. ) ;
#42928=LINE ( 'NONE', #69449, #13955 ) ;
#43145=FACE_OUTER_BOUND ( 'NONE', #72665, .T. ) ;
#43159=DIRECTION ( 'NONE',  ( -0.000000000000000000, 0.000000000000000000, 1.000000000000000000 ) ) ;
#43187=CONICAL_SURFACE ( 'NONE', #47230, 0.1181102362204724116, 0.7853981633974536081 ) ;
#43245=ORIENTED_EDGE ( 'NONE', *, *, #67561, .F. ) ;
#43282=DIRECTION ( 'NONE',  ( -1.734723475976806848E-16, -1.000000000000000000, 0.000000000000000000 ) ) ;
#43576=PLANE ( 'NONE',  #70737 ) ;
#43693=LINE ( 'NONE', #5008, #24665 ) ;
#43804=PLANE ( 'NONE',  #46127 ) ;
#43920=CIRCLE ( 'NONE', #29345, 0.09842519685039372024 ) ;
#43986=VECTOR ( 'NONE', #28090, 39.37007874015748143 ) ;
#44068=CARTESIAN_POINT ( 'NONE',  ( 0.1181102362204724532, 0.09842519685039372024, -1.432673802628665356E-17 ) ) ;
#44219=DIRECTION ( 'NONE',  ( 0.000000000000000000, -0.4999999999999998335, -0.8660254037844385966 ) ) ;
#44271=ORIENTED_EDGE ( 'NONE', *, *, #35758, .T. ) ;
#44504=VECTOR ( 'NONE', #70226, 39.37007874015748854 ) ;
#44512=DIRECTION ( 'NONE',  ( -1.000000000000000000, -0.000000000000000000, -0.000000000000000000 ) ) ;
#44650=DIRECTION ( 'NONE',  ( 0.000000000000000000, 0.8660254037844387076, -0.4999999999999998890 ) ) ;
#44759=CYLINDRICAL_SURFACE ( 'NONE', #33144, 0.1181102362204724116 ) ;
#44855=ORIENTED_EDGE ( 'NONE', *, *, #35758, .F. ) ;
#44952=ADVANCED_FACE ( 'NONE', ( #8194 ), #76965, .F. ) ;
#45304=ORIENTED_EDGE ( 'NONE', *, *, #78629, .T. ) ;
#45483=CARTESIAN_POINT ( 'NONE',  ( 0.2362204724409449064, 0.000000000000000000, 0.000000000000000000 ) ) ;
#45907=ORIENTED_EDGE ( 'NONE', *, *, #78379, .F. ) ;
#46041=ORIENTED_EDGE ( 'NONE', *, *, #64831, .F. ) ;
#46060=ADVANCED_FACE ( 'NONE', ( #35146, #35560 ), #43804, .F. ) ;
#46092=LINE ( 'NONE', #22096, #13878 ) ;
#46095=EDGE_CURVE ( 'NONE', #53271, #50299, #3137, .T. ) ;
#46127=AXIS2_PLACEMENT_3D ( 'NONE', #29654, #69508, #11857 ) ;
#46360=( GEOMETRIC_REPRESENTATION_CONTEXT ( 3 ) GLOBAL_UNCERTAINTY_ASSIGNED_CONTEXT ( ( #54574 ) ) GLOBAL_UNIT_ASSIGNED_CONTEXT ( ( #29310, #54137, #67624 ) ) REPRESENTATION_CONTEXT ( 'NONE', 'WORKASPACE' ) );
#46419=DIRECTION ( 'NONE',  ( 0.000000000000000000, -0.8660254037844387076, -0.4999999999999999445 ) ) ;
#46496=ADVANCED_FACE ( 'NONE', ( #20238 ), #6352, .F. ) ;
#46540=TOROIDAL_SURFACE ( 'NONE', #10280, 0.1279527559055117503, 0.009842519685039369942 ) ;
#46544=EDGE_CURVE ( 'NONE', #29401, #5577, #76242, .T. ) ;
#46771=VECTOR ( 'NONE', #50851, 39.37007874015748143 ) ;
#46974=DIRECTION ( 'NONE',  ( 0.000000000000000000, -1.000000000000000000, 1.734723475976806108E-16 ) ) ;
#46991=EDGE_CURVE ( 'NONE', #30272, #32285, #42120, .T. ) ;
#47024=CARTESIAN_POINT ( 'NONE',  ( 0.6889763779527560139, 1.446433227339393149E-17, -0.1181102362204724116 ) ) ;
#47038=EDGE_CURVE ( 'NONE', #17151, #22673, #40430, .T. ) ;
#47073=ORIENTED_EDGE ( 'NONE', *, *, #59455, .F. ) ;
#47230=AXIS2_PLACEMENT_3D ( 'NONE', #30842, #48960, #75890 ) ;
#47390=ORIENTED_EDGE ( 'NONE', *, *, #32695, .F. ) ;
#47572=CARTESIAN_POINT ( 'NONE',  ( -39.19291338582677753, 5.691349986800547090E-15, 0.000000000000000000 ) ) ;
#47712=DIRECTION ( 'NONE',  ( -1.000000000000000000, 1.445602896647338917E-16, -0.000000000000000000 ) ) ;
#47774=CARTESIAN_POINT ( 'NONE',  ( 0.01968503937007875723, 2.410722045565656378E-17, -0.1968503937007874405 ) ) ;
#47884=VERTEX_POINT ( 'NONE', #52100 ) ;
#48083=FACE_OUTER_BOUND ( 'NONE', #18628, .T. ) ;
#48127=ORIENTED_EDGE ( 'NONE', *, *, #79898, .T. ) ;
#48243=ORIENTED_EDGE ( 'NONE', *, *, #79898, .F. ) ;
#48423=VERTEX_POINT ( 'NONE', #33826 ) ;
#48543=SURFACE_STYLE_USAGE ( .BOTH. , #15760 ) ;
#48960=DIRECTION ( 'NONE',  ( -1.000000000000000000, -0.000000000000000000, -0.000000000000000000 ) ) ;
#48969=SHAPE_DEFINITION_REPRESENTATION ( #54067, #27201 ) ;
#49129=ORIENTED_EDGE ( 'NONE', *, *, #70912, .F. ) ;
#49346=DIRECTION ( 'NONE',  ( -1.000000000000000000, -0.000000000000000000, -0.000000000000000000 ) ) ;
#49469=VERTEX_POINT ( 'NONE', #24498 ) ;
#49555=EDGE_CURVE ( 'NONE', #11621, #15186, #42928, .T. ) ;
#49560=ORIENTED_EDGE ( 'NONE', *, *, #33065, .F. ) ;
#49734=FACE_OUTER_BOUND ( 'NONE', #13852, .T. ) ;
#49874=ORIENTED_EDGE ( 'NONE', *, *, #56663, .T. ) ;
#50193=FACE_OUTER_BOUND ( 'NONE', #78578, .T. ) ;
#50239=DIMENSIONAL_EXPONENTS ( 1.000000000000000000, 0.000000000000000000, 0.000000000000000000, 0.000000000000000000, 0.000000000000000000, 0.000000000000000000, 0.000000000000000000 ) ;
#50291=DIRECTION ( 'NONE',  ( -1.000000000000000000, -0.000000000000000000, -0.000000000000000000 ) ) ;
#50299=VERTEX_POINT ( 'NONE', #74854 ) ;
#50397=ORIENTED_EDGE ( 'NONE', *, *, #29128, .T. ) ;
#50599=LINE ( 'NONE', #10681, #25702 ) ;
#50851=DIRECTION ( 'NONE',  ( 0.000000000000000000, 1.000000000000000000, -1.734723475976805862E-16 ) ) ;
#51242=CYLINDRICAL_SURFACE ( 'NONE', #52031, 0.1968503937007874405 ) ;
#51518=DIRECTION ( 'NONE',  ( 1.000000000000000000, 0.000000000000000000, 0.000000000000000000 ) ) ;
#51535=ORIENTED_EDGE ( 'NONE', *, *, #4017, .F. ) ;
#51606=ORIENTED_EDGE ( 'NONE', *, *, #40415, .T. ) ;
#51697=VECTOR ( 'NONE', #50291, 39.37007874015748143 ) ;
#51714=VERTEX_POINT ( 'NONE', #59475 ) ;
#51751=CARTESIAN_POINT ( 'NONE',  ( 0.1181102362204724254, 0.04921259842519689481, -0.08523872084492506440 ) ) ;
#51936=ORIENTED_EDGE ( 'NONE', *, *, #35126, .F. ) ;
#52031=AXIS2_PLACEMENT_3D ( 'NONE', #26426, #44512, #13392 ) ;
#52100=CARTESIAN_POINT ( 'NONE',  ( 0.1181102362204724254, -0.04921259842519686706, -0.08523872084492506440 ) ) ;
#52135=EDGE_LOOP ( 'NONE', ( #44855, #83114, #31223, #39013 ) ) ;
#52211=ADVANCED_FACE ( 'NONE', ( #48083 ), #9987, .T. ) ;
#52311=FACE_OUTER_BOUND ( 'NONE', #67587, .T. ) ;
#52522=ADVANCED_FACE ( 'NONE', ( #49734 ), #5128, .T. ) ;
#52608=EDGE_CURVE ( 'NONE', #32285, #30272, #66405, .T. ) ;
#52795=CARTESIAN_POINT ( 'NONE',  ( 1.080276388343102000E-18, 0.000000000000000000, -0.1771653543307086798 ) ) ;
#52825=EDGE_LOOP ( 'NONE', ( #4035, #12579, #46041, #47390, #31456, #57083 ) ) ;
#53186=VECTOR ( 'NONE', #79340, 39.37007874015748854 ) ;
#53208=CARTESIAN_POINT ( 'NONE',  ( 0.1181102362204724532, 0.09842519685039373412, 4.268512490100411895E-17 ) ) ;
#53271=VERTEX_POINT ( 'NONE', #82877 ) ;
#53490=ADVANCED_BREP_SHAPE_REPRESENTATION ( '', ( #33421, #22098 ), #46360 ) ;
#53814=ORIENTED_EDGE ( 'NONE', *, *, #39057, .T. ) ;
#53956=( GEOMETRIC_REPRESENTATION_CONTEXT ( 3 ) GLOBAL_UNCERTAINTY_ASSIGNED_CONTEXT ( ( #39464 ) ) GLOBAL_UNIT_ASSIGNED_CONTEXT ( ( #73830, #72985, #10266 ) ) REPRESENTATION_CONTEXT ( 'NONE', 'WORKASPACE' ) );
#54019=VERTEX_POINT ( 'NONE', #60933 ) ;
#54030=ORIENTED_EDGE ( 'NONE', *, *, #56216, .T. ) ;
#54067=PRODUCT_DEFINITION_SHAPE ( 'NONE', 'NONE',  #23368 ) ;
#54069=DIRECTION ( 'NONE',  ( 1.000000000000000000, 0.000000000000000000, 0.000000000000000000 ) ) ;
#54137=( NAMED_UNIT ( * ) PLANE_ANGLE_UNIT ( ) SI_UNIT ( $, .RADIAN. ) );
#54287=DIRECTION ( 'NONE',  ( -1.000000000000000000, -0.000000000000000000, -0.000000000000000000 ) ) ;
#54367=LINE ( 'NONE', #68268, #62762 ) ;
#54475=CARTESIAN_POINT ( 'NONE',  ( 0.6889763779527560139, 1.446433227339393149E-17, -0.1181102362204724116 ) ) ;
#54554=( LENGTH_UNIT ( ) NAMED_UNIT ( * ) SI_UNIT ( $, .METRE. ) );
#54574=UNCERTAINTY_MEASURE_WITH_UNIT (LENGTH_MEASURE( 1.000000000000000082E-05 ), #29310, 'distance_accuracy_value', 'NONE');
#54673=DIRECTION ( 'NONE',  ( 1.000000000000000000, -1.445602896647338917E-16, 0.000000000000000000 ) ) ;
#54979=FACE_OUTER_BOUND ( 'NONE', #61226, .T. ) ;
#55200=DIRECTION ( 'NONE',  ( 0.000000000000000000, -0.4999999999999998335, 0.8660254037844385966 ) ) ;
#55213=CIRCLE ( 'NONE', #63270, 0.09842519685039372024 ) ;
#55218=CARTESIAN_POINT ( 'NONE',  ( 0.1181102362204724532, -0.04921259842519688094, 0.08523872084492505052 ) ) ;
#55260=ORIENTED_EDGE ( 'NONE', *, *, #33761, .T. ) ;
#55337=EDGE_CURVE ( 'NONE', #49469, #29384, #62420, .T. ) ;
#55361=ORIENTED_EDGE ( 'NONE', *, *, #77077, .F. ) ;
#55459=CARTESIAN_POINT ( 'NONE',  ( 0.1181102362204724532, 0.04921259842519689481, -0.08523872084492506440 ) ) ;
#55820=CARTESIAN_POINT ( 'NONE',  ( 0.2460629921259842590, 1.566969329617675860E-17, -0.1279527559055117503 ) ) ;
#55960=CARTESIAN_POINT ( 'NONE',  ( 0.1181102362204724532, -0.04921259842519685318, -0.08523872084492505052 ) ) ;
#55974=DIRECTION ( 'NONE',  ( 0.000000000000000000, -0.4999999999999998335, -0.8660254037844385966 ) ) ;
#56130=TOROIDAL_SURFACE ( 'NONE', #69546, 0.1279527559055117503, 0.009842519685039369942 ) ;
#56216=EDGE_CURVE ( 'NONE', #60118, #80363, #26185, .T. ) ;
#56356=ORIENTED_EDGE ( 'NONE', *, *, #71970, .F. ) ;
#56458=CARTESIAN_POINT ( 'NONE',  ( 0.1181102362204724116, -0.09842519685039370636, 0.000000000000000000 ) ) ;
#56647=CIRCLE ( 'NONE', #41882, 0.1968503937007874405 ) ;
#56663=EDGE_CURVE ( 'NONE', #49469, #80363, #30117, .T. ) ;
#56890=DIRECTION ( 'NONE',  ( 0.000000000000000000, 0.000000000000000000, 1.000000000000000000 ) ) ;
#57083=ORIENTED_EDGE ( 'NONE', *, *, #76734, .F. ) ;
#57170=CARTESIAN_POINT ( 'NONE',  ( 0.1771653543307086798, 0.000000000000000000, 0.000000000000000000 ) ) ;
#57323=AXIS2_PLACEMENT_3D ( 'NONE', #68412, #10344, #11163 ) ;
#57385=AXIS2_PLACEMENT_3D ( 'NONE', #72057, #33343, #6818 ) ;
#57428=DIRECTION ( 'NONE',  ( -1.000000000000000000, -0.000000000000000000, -0.000000000000000000 ) ) ;
#57663=AXIS2_PLACEMENT_3D ( 'NONE', #30210, #69352, #11284 ) ;
#58405=FACE_OUTER_BOUND ( 'NONE', #20049, .T. ) ;
#58749=CARTESIAN_POINT ( 'NONE',  ( 0.1181102362204724254, 8.537024980200824098E-18, 0.000000000000000000 ) ) ;
#59101=DIRECTION ( 'NONE',  ( -1.000000000000000000, -0.000000000000000000, -0.000000000000000000 ) ) ;
#59109=ORIENTED_EDGE ( 'NONE', *, *, #30503, .T. ) ;
#59211=ORIENTED_EDGE ( 'NONE', *, *, #76734, .T. ) ;
#59332=DIRECTION ( 'NONE',  ( -1.734723475976806848E-16, -1.000000000000000000, 0.000000000000000000 ) ) ;
#59365=COLOUR_RGB ( '', 0.40784314, 0.44705882, 0.49803922) ;
#59378=ORIENTED_EDGE ( 'NONE', *, *, #46991, .F. ) ;
#59425=PRODUCT ( 'Chuck Body Assembly Bolts', 'Chuck Body Assembly Bolts', '', ( #66693 ) ) ;
#59455=EDGE_CURVE ( 'NONE', #47884, #17151, #62000, .T. ) ;
#59475=CARTESIAN_POINT ( 'NONE',  ( 0.1181102362204724254, 0.04921259842519697808, 0.08523872084492500889 ) ) ;
#59590=ORIENTED_EDGE ( 'NONE', *, *, #55337, .T. ) ;
#59657=DIRECTION ( 'NONE',  ( -0.7071067811865437980, 8.659560562354978464E-17, -0.7071067811865512365 ) ) ;
#60118=VERTEX_POINT ( 'NONE', #76294 ) ;
#60355=DIRECTION ( 'NONE',  ( -1.734723475976806848E-16, -1.000000000000000000, 0.000000000000000000 ) ) ;
#60488=EDGE_CURVE ( 'NONE', #66895, #77098, #35911, .T. ) ;
#60585=CARTESIAN_POINT ( 'NONE',  ( 0.1181102362204724532, -0.04921259842519688094, 0.08523872084492505052 ) ) ;
#60615=CARTESIAN_POINT ( 'NONE',  ( 0.000000000000000000, -0.04921259842519685318, -0.08523872084492505052 ) ) ;
#60628=ORIENTED_EDGE ( 'NONE', *, *, #13591, .T. ) ;
#60697=MECHANICAL_DESIGN_GEOMETRIC_PRESENTATION_REPRESENTATION('',(#5590),#53956);
#60700=FACE_OUTER_BOUND ( 'NONE', #67788, .T. ) ;
#60933=CARTESIAN_POINT ( 'NONE',  ( 0.1771653543307086798, 0.000000000000000000, 0.000000000000000000 ) ) ;
#60994=PLANE ( 'NONE',  #61429 ) ;
#61126=DIRECTION ( 'NONE',  ( -1.000000000000000000, -0.000000000000000000, -0.000000000000000000 ) ) ;
#61226=EDGE_LOOP ( 'NONE', ( #77238, #51535, #29153, #19733 ) ) ;
#61429=AXIS2_PLACEMENT_3D ( 'NONE', #3343, #54673, #80385 ) ;
#61602=ADVANCED_FACE ( 'NONE', ( #920 ), #26577, .F. ) ;
#61941=DIRECTION ( 'NONE',  ( 1.000000000000000000, 0.000000000000000000, 0.000000000000000000 ) ) ;
#62000=LINE ( 'NONE', #73400, #953 ) ;
#62070=EDGE_CURVE ( 'NONE', #47884, #66895, #17287, .T. ) ;
#62108=CARTESIAN_POINT ( 'NONE',  ( 0.000000000000000000, 0.000000000000000000, 0.000000000000000000 ) ) ;
#62182=AXIS2_PLACEMENT_3D ( 'NONE', #72581, #633, #13680 ) ;
#62196=VERTEX_POINT ( 'NONE', #31115 ) ;
#62381=ADVANCED_FACE ( 'NONE', ( #24391 ), #56130, .F. ) ;
#62420=CIRCLE ( 'NONE', #73191, 0.1181102362204724116 ) ;
#62762=VECTOR ( 'NONE', #3040, 39.37007874015748143 ) ;
#62940=DIRECTION ( 'NONE',  ( -1.000000000000000000, -0.000000000000000000, -0.000000000000000000 ) ) ;
#63123=EDGE_LOOP ( 'NONE', ( #51936, #59109, #1509, #50397, #35309 ) ) ;
#63270=AXIS2_PLACEMENT_3D ( 'NONE', #35509, #29602, #11082 ) ;
#63631=ORIENTED_EDGE ( 'NONE', *, *, #62070, .T. ) ;
#63718=VECTOR ( 'NONE', #46974, 39.37007874015748143 ) ;
#63882=PRODUCT_DEFINITION_CONTEXT ( 'detailed design', #75624, 'design' ) ;
#63968=CIRCLE ( 'NONE', #68021, 0.1771653543307086798 ) ;
#64248=ORIENTED_EDGE ( 'NONE', *, *, #52608, .T. ) ;
#64349=ORIENTED_EDGE ( 'NONE', *, *, #40447, .T. ) ;
#64430=CARTESIAN_POINT ( 'NONE',  ( 0.000000000000000000, 0.09842519685039372024, -1.432673802628665356E-17 ) ) ;
#64448=ORIENTED_EDGE ( 'NONE', *, *, #42687, .T. ) ;
#64636=EDGE_LOOP ( 'NONE', ( #13665, #1141, #9193, #17052 ) ) ;
#64784=ORIENTED_EDGE ( 'NONE', *, *, #16008, .F. ) ;
#64831=EDGE_CURVE ( 'NONE', #48423, #80, #31503, .T. ) ;
#65021=DIRECTION ( 'NONE',  ( -1.000000000000000000, -0.000000000000000000, -0.000000000000000000 ) ) ;
#65419=CIRCLE ( 'NONE', #29118, 0.009842519685039378616 ) ;
#65438=ORIENTED_EDGE ( 'NONE', *, *, #56216, .F. ) ;
#65453=DIRECTION ( 'NONE',  ( 0.000000000000000000, 0.000000000000000000, 1.000000000000000000 ) ) ;
#65852=CARTESIAN_POINT ( 'NONE',  ( 0.01968503937007875723, 0.000000000000000000, 0.000000000000000000 ) ) ;
#65944=DIRECTION ( 'NONE',  ( 0.000000000000000000, 0.000000000000000000, -1.000000000000000000 ) ) ;
#65978=CARTESIAN_POINT ( 'NONE',  ( 0.1771653543307086798, 0.000000000000000000, 0.000000000000000000 ) ) ;
#66326=CIRCLE ( 'NONE', #23353, 0.09842519685039372024 ) ;
#66373=DIRECTION ( 'NONE',  ( -0.000000000000000000, 1.734723475976805615E-16, 1.000000000000000000 ) ) ;
#66405=CIRCLE ( 'NONE', #70405, 0.1279527559055117503 ) ;
#66680=VECTOR ( 'NONE', #59657, 39.37007874015748143 ) ;
#66693=PRODUCT_CONTEXT ( 'NONE', #12679, 'mechanical' ) ;
#66834=DIRECTION ( 'NONE',  ( -1.000000000000000000, -0.000000000000000000, -0.000000000000000000 ) ) ;
#66895=VERTEX_POINT ( 'NONE', #56458 ) ;
#67145=VERTEX_POINT ( 'NONE', #47774 ) ;
#67183=CARTESIAN_POINT ( 'NONE',  ( 0.000000000000000000, 0.04921259842519689481, -0.08523872084492506440 ) ) ;
#67191=ORIENTED_EDGE ( 'NONE', *, *, #33761, .F. ) ;
#67386=DIRECTION ( 'NONE',  ( 1.445602896647338917E-16, 1.000000000000000000, 0.000000000000000000 ) ) ;
#67442=PLANE ( 'NONE',  #23600 ) ;
#67561=EDGE_CURVE ( 'NONE', #77098, #51714, #43920, .T. ) ;
#67587=EDGE_LOOP ( 'NONE', ( #3940, #23752, #71857, #21219 ) ) ;
#67624=( NAMED_UNIT ( * ) SI_UNIT ( $, .STERADIAN. ) SOLID_ANGLE_UNIT ( ) );
#67654=DIRECTION ( 'NONE',  ( -0.000000000000000000, 1.000000000000000000, 1.224646799147353207E-16 ) ) ;
#67655=DIRECTION ( 'NONE',  ( 0.000000000000000000, 0.000000000000000000, 1.000000000000000000 ) ) ;
#67788=EDGE_LOOP ( 'NONE', ( #617, #35687, #3992, #64448 ) ) ;
#68021=AXIS2_PLACEMENT_3D ( 'NONE', #71738, #59101, #14513 ) ;
#68037=SHAPE_REPRESENTATION_RELATIONSHIP ( 'NONE' , 'NONE' ,  #27201, #53490 ) ;
#68164=CARTESIAN_POINT ( 'NONE',  ( 0.000000000000000000, 0.000000000000000000, 0.000000000000000000 ) ) ;
#68223=ORIENTED_EDGE ( 'NONE', *, *, #70912, .T. ) ;
#68268=CARTESIAN_POINT ( 'NONE',  ( 0.000000000000000000, 2.410722045565656378E-17, -0.1968503937007874405 ) ) ;
#68412=CARTESIAN_POINT ( 'NONE',  ( 0.2460629921259843422, 0.000000000000000000, 0.000000000000000000 ) ) ;
#68615=DIRECTION ( 'NONE',  ( 1.000000000000000000, -1.445602896647338917E-16, 0.000000000000000000 ) ) ;
#68750=VECTOR ( 'NONE', #38496, 39.37007874015748854 ) ;
#68912=VECTOR ( 'NONE', #77032, 39.37007874015748143 ) ;
#69105=CARTESIAN_POINT ( 'NONE',  ( 0.1181102362204724532, 0.09842519685039372024, 0.000000000000000000 ) ) ;
#69352=DIRECTION ( 'NONE',  ( 1.000000000000000000, -1.445602896647338917E-16, 0.000000000000000000 ) ) ;
#69430=EDGE_LOOP ( 'NONE', ( #45304, #55361 ) ) ;
#69449=CARTESIAN_POINT ( 'NONE',  ( 0.1181102362204724532, 0.09842519685039372024, -1.432673802628665356E-17 ) ) ;
#69508=DIRECTION ( 'NONE',  ( -1.000000000000000000, 0.000000000000000000, -0.000000000000000000 ) ) ;
#69519=DIRECTION ( 'NONE',  ( 1.000000000000000000, -1.445602896647338917E-16, 0.000000000000000000 ) ) ;
#69545=ORIENTED_EDGE ( 'NONE', *, *, #46095, .F. ) ;
#69546=AXIS2_PLACEMENT_3D ( 'NONE', #80844, #82078, #35799 ) ;
#69709=DIRECTION ( 'NONE',  ( 0.000000000000000000, 0.4999999999999998335, -0.8660254037844385966 ) ) ;
#70041=DIRECTION ( 'NONE',  ( -1.000000000000000000, -0.000000000000000000, -0.000000000000000000 ) ) ;
#70162=PLANE ( 'NONE',  #57663 ) ;
#70205=ADVANCED_FACE ( 'NONE', ( #16828 ), #9672, .T. ) ;
#70226=DIRECTION ( 'NONE',  ( -0.5144957554275264577, 0.8574929257125440962, 1.050125966765366037E-16 ) ) ;
#70322=CARTESIAN_POINT ( 'NONE',  ( 0.1181102362204724532, 0.04921259842519689481, -0.08523872084492506440 ) ) ;
#70405=AXIS2_PLACEMENT_3D ( 'NONE', #74097, #16859, #72846 ) ;
#70589=CARTESIAN_POINT ( 'NONE',  ( 0.000000000000000000, 0.04921259842519689481, 0.08523872084492503665 ) ) ;
#70661=VERTEX_POINT ( 'NONE', #38634 ) ;
#70737=AXIS2_PLACEMENT_3D ( 'NONE', #4469, #81505, #23827 ) ;
#70912=EDGE_CURVE ( 'NONE', #53271, #29384, #72716, .T. ) ;
#70964=CARTESIAN_POINT ( 'NONE',  ( 0.000000000000000000, 0.000000000000000000, 0.1968503937007874405 ) ) ;
#71147=VECTOR ( 'NONE', #81168, 39.37007874015748143 ) ;
#71180=DIRECTION ( 'NONE',  ( -1.000000000000000000, -0.000000000000000000, -0.000000000000000000 ) ) ;
#71417=ORIENTED_EDGE ( 'NONE', *, *, #64831, .T. ) ;
#71495=FACE_OUTER_BOUND ( 'NONE', #39510, .T. ) ;
#71688=AXIS2_PLACEMENT_3D ( 'NONE', #41863, #54069, #16632 ) ;
#71738=CARTESIAN_POINT ( 'NONE',  ( 1.080276388343102000E-18, 0.000000000000000000, 0.000000000000000000 ) ) ;
#71786=AXIS2_PLACEMENT_3D ( 'NONE', #47572, #39607, #2563 ) ;
#71857=ORIENTED_EDGE ( 'NONE', *, *, #62070, .F. ) ;
#71970=EDGE_CURVE ( 'NONE', #32372, #81967, #19606, .T. ) ;
#72057=CARTESIAN_POINT ( 'NONE',  ( 0.1181102362204724254, 8.537024980200824098E-18, 0.000000000000000000 ) ) ;
#72111=DIRECTION ( 'NONE',  ( 0.000000000000000000, 0.4999999999999998890, -0.8660254037844385966 ) ) ;
#72395=CARTESIAN_POINT ( 'NONE',  ( 1.080276388343102000E-18, 0.000000000000000000, -0.1771653543307086798 ) ) ;
#72581=CARTESIAN_POINT ( 'NONE',  ( -39.19291338582677753, 5.691349986800547090E-15, 0.000000000000000000 ) ) ;
#72597=ADVANCED_FACE ( 'NONE', ( #10554 ), #16047, .T. ) ;
#72665=EDGE_LOOP ( 'NONE', ( #59590, #17296, #76281, #38488 ) ) ;
#72716=LINE ( 'NONE', #47024, #66680 ) ;
#72846=DIRECTION ( 'NONE',  ( 0.000000000000000000, 0.000000000000000000, 1.000000000000000000 ) ) ;
#72985=( NAMED_UNIT ( * ) PLANE_ANGLE_UNIT ( ) SI_UNIT ( $, .RADIAN. ) );
#73191=AXIS2_PLACEMENT_3D ( 'NONE', #81776, #49346, #56890 ) ;
#73221=LINE ( 'NONE', #60585, #9051 ) ;
#73331=ADVANCED_FACE ( 'NONE', ( #1605 ), #73562, .T. ) ;
#73400=CARTESIAN_POINT ( 'NONE',  ( 0.1181102362204724532, -0.04921259842519685318, -0.08523872084492505052 ) ) ;
#73412=LENGTH_MEASURE_WITH_UNIT ( LENGTH_MEASURE( 0.02539999999999999897 ), #42231 );
#73512=CARTESIAN_POINT ( 'NONE',  ( 0.2460629921259842590, 0.000000000000000000, 0.1279527559055117503 ) ) ;
#73562=PLANE ( 'NONE',  #11639 ) ;
#73731=EDGE_CURVE ( 'NONE', #32285, #60118, #65419, .T. ) ;
#73768=FACE_BOUND ( 'NONE', #52825, .T. ) ;
#73827=DIRECTION ( 'NONE',  ( 0.000000000000000000, 0.000000000000000000, 1.000000000000000000 ) ) ;
#73830=( CONVERSION_BASED_UNIT ( 'INCH', #73412 ) LENGTH_UNIT ( ) NAMED_UNIT ( #17997 ) );
#73922=ORIENTED_EDGE ( 'NONE', *, *, #34666, .T. ) ;
#74097=CARTESIAN_POINT ( 'NONE',  ( 0.2362204724409449064, 0.000000000000000000, 0.000000000000000000 ) ) ;
#74175=DIRECTION ( 'NONE',  ( -0.000000000000000000, 0.8660254037844387076, 0.4999999999999998890 ) ) ;
#74339=DIRECTION ( 'NONE',  ( -1.000000000000000000, -0.000000000000000000, -0.000000000000000000 ) ) ;
#74539=ORIENTED_EDGE ( 'NONE', *, *, #30503, .F. ) ;
#74750=EDGE_LOOP ( 'NONE', ( #10052, #80161, #22676, #73922 ) ) ;
#74789=EDGE_CURVE ( 'NONE', #66895, #77098, #46092, .T. ) ;
#74852=AXIS2_PLACEMENT_3D ( 'NONE', #75273, #5785, #4551 ) ;
#74854=CARTESIAN_POINT ( 'NONE',  ( 0.7086614173228347191, 0.000000000000000000, 0.09842519685039344268 ) ) ;
#74900=CARTESIAN_POINT ( 'NONE',  ( 0.1181102362204724254, 8.537024980200824098E-18, 0.000000000000000000 ) ) ;
#74947=CARTESIAN_POINT ( 'NONE',  ( 0.1181102362204724532, 0.09842519685039372024, 0.000000000000000000 ) ) ;
#75164=CARTESIAN_POINT ( 'NONE',  ( 0.2460629921259843422, 0.000000000000000000, 0.1181102362204723977 ) ) ;
#75262=LINE ( 'NONE', #55459, #71147 ) ;
#75273=CARTESIAN_POINT ( 'NONE',  ( 0.7086614173228347191, 0.000000000000000000, 0.000000000000000000 ) ) ;
#75581=DIRECTION ( 'NONE',  ( 0.000000000000000000, 0.000000000000000000, 1.000000000000000000 ) ) ;
#75624=APPLICATION_CONTEXT ( 'automotive_design' ) ;
#75720=CARTESIAN_POINT ( 'NONE',  ( 0.1181102362204724532, -0.04921259842519688094, 0.08523872084492505052 ) ) ;
#75890=DIRECTION ( 'NONE',  ( 0.000000000000000000, 0.000000000000000000, 1.000000000000000000 ) ) ;
#76030=CARTESIAN_POINT ( 'NONE',  ( 0.1181102362204724532, 0.04921259842519689481, 0.08523872084492503665 ) ) ;
#76061=ORIENTED_EDGE ( 'NONE', *, *, #67561, .T. ) ;
#76242=LINE ( 'NONE', #64430, #20623 ) ;
#76281=ORIENTED_EDGE ( 'NONE', *, *, #39057, .F. ) ;
#76294=CARTESIAN_POINT ( 'NONE',  ( 0.2460629921259843422, 1.506701278478534659E-17, -0.1181102362204724116 ) ) ;
#76734=EDGE_CURVE ( 'NONE', #5577, #17151, #43693, .T. ) ;
#76910=EDGE_LOOP ( 'NONE', ( #64349, #77267 ) ) ;
#76965=CONICAL_SURFACE ( 'NONE', #62182, 65.61679790026244063, 1.030376826524312284 ) ;
#77032=DIRECTION ( 'NONE',  ( -1.000000000000000000, -0.000000000000000000, -0.000000000000000000 ) ) ;
#77077=EDGE_CURVE ( 'NONE', #51714, #11621, #66326, .T. ) ;
#77098=VERTEX_POINT ( 'NONE', #75720 ) ;
#77129=VECTOR ( 'NONE', #69709, 39.37007874015748854 ) ;
#77147=AXIS2_PLACEMENT_3D ( 'NONE', #35466, #42184, #80518 ) ;
#77238=ORIENTED_EDGE ( 'NONE', *, *, #32695, .T. ) ;
#77267=ORIENTED_EDGE ( 'NONE', *, *, #22774, .T. ) ;
#77454=DIRECTION ( 'NONE',  ( -1.000000000000000000, 1.445602896647338917E-16, -0.000000000000000000 ) ) ;
#77933=DIRECTION ( 'NONE',  ( 0.000000000000000000, 0.4999999999999998335, 0.8660254037844385966 ) ) ;
#77946=ORIENTED_EDGE ( 'NONE', *, *, #79009, .F. ) ;
#78379=EDGE_CURVE ( 'NONE', #29384, #49469, #467, .T. ) ;
#78532=CIRCLE ( 'NONE', #42217, 0.009842519685039378616 ) ;
#78578=EDGE_LOOP ( 'NONE', ( #69545, #68223, #37436, #67191 ) ) ;
#78629=EDGE_CURVE ( 'NONE', #51714, #11621, #82346, .T. ) ;
#78939=CARTESIAN_POINT ( 'NONE',  ( 1.080276388343102000E-18, 0.09842519685039372024, -8.537024980200822558E-18 ) ) ;
#79009=EDGE_CURVE ( 'NONE', #70661, #32372, #12662, .T. ) ;
#79052=ADVANCED_FACE ( 'NONE', ( #21086 ), #19317, .F. ) ;
#79117=ORIENTED_EDGE ( 'NONE', *, *, #6402, .F. ) ;
#79139=LINE ( 'NONE', #72395, #35907 ) ;
#79340=DIRECTION ( 'NONE',  ( 0.7071067811865474617, 8.659560562354932858E-17, 0.7071067811865474617 ) ) ;
#79579=EDGE_CURVE ( 'NONE', #30272, #80363, #78532, .T. ) ;
#79688=CARTESIAN_POINT ( 'NONE',  ( 0.000000000000000000, 1.446433227339393149E-17, -0.1181102362204724116 ) ) ;
#79786=ORIENTED_EDGE ( 'NONE', *, *, #15246, .F. ) ;
#79898=EDGE_CURVE ( 'NONE', #15186, #47884, #22974, .T. ) ;
#80161=ORIENTED_EDGE ( 'NONE', *, *, #79009, .T. ) ;
#80363=VERTEX_POINT ( 'NONE', #75164 ) ;
#80385=DIRECTION ( 'NONE',  ( 1.445602896647338917E-16, 1.000000000000000000, 0.000000000000000000 ) ) ;
#80518=DIRECTION ( 'NONE',  ( 0.000000000000000000, 0.000000000000000000, -1.000000000000000000 ) ) ;
#80675=PLANE ( 'NONE',  #9779 ) ;
#80844=CARTESIAN_POINT ( 'NONE',  ( 0.2460629921259842590, 0.000000000000000000, 0.000000000000000000 ) ) ;
#80857=ORIENTED_EDGE ( 'NONE', *, *, #77077, .T. ) ;
#80964=VECTOR ( 'NONE', #11034, 39.37007874015748143 ) ;
#81077=VECTOR ( 'NONE', #27801, 39.37007874015748854 ) ;
#81168=DIRECTION ( 'NONE',  ( -1.000000000000000000, -0.000000000000000000, -0.000000000000000000 ) ) ;
#81414=ADVANCED_FACE ( 'NONE', ( #19871 ), #40910, .T. ) ;
#81422=AXIS2_PLACEMENT_3D ( 'NONE', #29130, #74175, #55200 ) ;
#81505=DIRECTION ( 'NONE',  ( 0.000000000000000000, -0.8660254037844388186, 0.4999999999999997224 ) ) ;
#81776=CARTESIAN_POINT ( 'NONE',  ( 0.6889763779527560139, 0.000000000000000000, 0.000000000000000000 ) ) ;
#81899=CARTESIAN_POINT ( 'NONE',  ( 0.2362204724409449064, 0.000000000000000000, 0.000000000000000000 ) ) ;
#81967=VERTEX_POINT ( 'NONE', #3654 ) ;
#82003=CARTESIAN_POINT ( 'NONE',  ( 1.080276388343102000E-18, 0.000000000000000000, 0.000000000000000000 ) ) ;
#82078=DIRECTION ( 'NONE',  ( -1.000000000000000000, -0.000000000000000000, -0.000000000000000000 ) ) ;
#82100=AXIS2_PLACEMENT_3D ( 'NONE', #28777, #22470, #73827 ) ;
#82346=LINE ( 'NONE', #76030, #77129 ) ;
#82409=DIRECTION ( 'NONE',  ( -1.000000000000000000, -0.000000000000000000, -0.000000000000000000 ) ) ;
#82474=VERTEX_POINT ( 'NONE', #52795 ) ;
#82490=ORIENTED_EDGE ( 'NONE', *, *, #21410, .F. ) ;
#82702=EDGE_LOOP ( 'NONE', ( #49129, #41892, #55260, #45907 ) ) ;
#82877=CARTESIAN_POINT ( 'NONE',  ( 0.7086614173228347191, 1.325897125061109051E-17, -0.09842519685039344268 ) ) ;
#83114=ORIENTED_EDGE ( 'NONE', *, *, #40447, .F. ) ;
ENDSEC;
END-ISO-10303-21;
